ISO-10303-21;
HEADER;
/* Generated by software containing ST-Developer
 * from STEP Tools, Inc. (www.steptools.com) 
 */

FILE_DESCRIPTION(
/* description */ ('Timing belt drive module 2 mm Pitch Timing 20T-40T'),

/* implementation_level */ '2;1');

FILE_NAME(
/* name */ 'M4 clamp nut.step',
/* time_stamp */ '2026-10-28T03:25:12-07:00',
/* author */ (''),
/* organization */ (''),
/* preprocessor_version */ 'ST-DEVELOPER v20.2',
/* originating_system */ 'Autodesk Translation Framework v15.17.0.0',
/* authorisation */ '');

FILE_SCHEMA (('AUTOMOTIVE_DESIGN { 1 0 10303 214 3 1 1 }'));
ENDSEC;

DATA;
#10=MECHANICAL_DESIGN_GEOMETRIC_PRESENTATION_REPRESENTATION('',(#532),#17830);
#446=SHAPE_REPRESENTATION_RELATIONSHIP('SRR','None',#18016,#489);
#489=ADVANCED_BREP_SHAPE_REPRESENTATION('',(#590),#17791);
#532=STYLED_ITEM('',(#18324),#590);
#590=MANIFOLD_SOLID_BREP('Body1',#8989);
#691=FACE_BOUND('',#1650,.T.);
#692=FACE_BOUND('',#1652,.T.);
#831=PLANE('',#9751);
#832=PLANE('',#9752);
#1072=FACE_OUTER_BOUND('',#1647,.T.);
#1073=FACE_OUTER_BOUND('',#1648,.T.);
#1074=FACE_OUTER_BOUND('',#1649,.T.);
#1075=FACE_OUTER_BOUND('',#1651,.T.);
#1647=EDGE_LOOP('',(#6313,#6314,#6315,#6316));
#1648=EDGE_LOOP('',(#6317,#6318,#6319,#6320));
#1649=EDGE_LOOP('',(#6321));
#1650=EDGE_LOOP('',(#6322));
#1651=EDGE_LOOP('',(#6323));
#1652=EDGE_LOOP('',(#6324));
#2248=CIRCLE('',#9746,0.165);
#2249=CIRCLE('',#9747,0.165);
#2250=CIRCLE('',#9749,0.4);
#2251=CIRCLE('',#9750,0.4);
#2952=LINE('',#14448,#3430);
#2953=LINE('',#14454,#3431);
#3430=VECTOR('',#11433,0.165);
#3431=VECTOR('',#11440,0.4);
#3926=VERTEX_POINT('',#14445);
#3927=VERTEX_POINT('',#14447);
#3928=VERTEX_POINT('',#14451);
#3929=VERTEX_POINT('',#14453);
#4839=EDGE_CURVE('',#3926,#3926,#2248,.T.);
#4840=EDGE_CURVE('',#3926,#3927,#2952,.T.);
#4841=EDGE_CURVE('',#3927,#3927,#2249,.T.);
#4842=EDGE_CURVE('',#3928,#3928,#2250,.T.);
#4843=EDGE_CURVE('',#3928,#3929,#2953,.T.);
#4844=EDGE_CURVE('',#3929,#3929,#2251,.T.);
#6313=ORIENTED_EDGE('',*,*,#4839,.F.);
#6314=ORIENTED_EDGE('',*,*,#4840,.T.);
#6315=ORIENTED_EDGE('',*,*,#4841,.T.);
#6316=ORIENTED_EDGE('',*,*,#4840,.F.);
#6317=ORIENTED_EDGE('',*,*,#4842,.F.);
#6318=ORIENTED_EDGE('',*,*,#4843,.T.);
#6319=ORIENTED_EDGE('',*,*,#4844,.T.);
#6320=ORIENTED_EDGE('',*,*,#4843,.F.);
#6321=ORIENTED_EDGE('',*,*,#4842,.T.);
#6322=ORIENTED_EDGE('',*,*,#4839,.T.);
#6323=ORIENTED_EDGE('',*,*,#4844,.F.);
#6324=ORIENTED_EDGE('',*,*,#4841,.F.);
#8233=CYLINDRICAL_SURFACE('',#9745,0.165);
#8234=CYLINDRICAL_SURFACE('',#9748,0.4);
#8570=ADVANCED_FACE('',(#1072),#8233,.F.);
#8571=ADVANCED_FACE('',(#1073),#8234,.T.);
#8572=ADVANCED_FACE('',(#1074,#691),#831,.T.);
#8573=ADVANCED_FACE('',(#1075,#692),#832,.F.);
#8989=CLOSED_SHELL('',(#8570,#8571,#8572,#8573));
#9744=AXIS2_PLACEMENT_3D('',#14443,#11427,#11428);
#9745=AXIS2_PLACEMENT_3D('',#14444,#11429,#11430);
#9746=AXIS2_PLACEMENT_3D('',#14446,#11431,#11432);
#9747=AXIS2_PLACEMENT_3D('',#14449,#11434,#11435);
#9748=AXIS2_PLACEMENT_3D('',#14450,#11436,#11437);
#9749=AXIS2_PLACEMENT_3D('',#14452,#11438,#11439);
#9750=AXIS2_PLACEMENT_3D('',#14455,#11441,#11442);
#9751=AXIS2_PLACEMENT_3D('',#14456,#11443,#11444);
#9752=AXIS2_PLACEMENT_3D('',#14457,#11445,#11446);
#11427=DIRECTION('axis',(0.,0.,1.));
#11428=DIRECTION('refdir',(1.,0.,0.));
#11429=DIRECTION('center_axis',(0.,0.,1.));
#11430=DIRECTION('ref_axis',(1.,0.,0.));
#11431=DIRECTION('center_axis',(0.,0.,-1.));
#11432=DIRECTION('ref_axis',(1.,0.,0.));
#11433=DIRECTION('',(0.,0.,-1.));
#11434=DIRECTION('center_axis',(0.,0.,-1.));
#11435=DIRECTION('ref_axis',(1.,0.,0.));
#11436=DIRECTION('center_axis',(0.,0.,1.));
#11437=DIRECTION('ref_axis',(1.,0.,0.));
#11438=DIRECTION('center_axis',(0.,0.,1.));
#11439=DIRECTION('ref_axis',(1.,0.,0.));
#11440=DIRECTION('',(0.,0.,-1.));
#11441=DIRECTION('center_axis',(0.,0.,1.));
#11442=DIRECTION('ref_axis',(1.,0.,0.));
#11443=DIRECTION('center_axis',(0.,0.,1.));
#11444=DIRECTION('ref_axis',(1.,0.,0.));
#11445=DIRECTION('center_axis',(0.,0.,1.));
#11446=DIRECTION('ref_axis',(1.,0.,0.));
#14443=CARTESIAN_POINT('',(0.,0.,0.));
#14444=CARTESIAN_POINT('Origin',(4.17091003018116,-1.,-1.6));
#14445=CARTESIAN_POINT('',(4.00591003018116,-1.,-1.2));
#14446=CARTESIAN_POINT('Origin',(4.17091003018116,-1.,-1.2));
#14447=CARTESIAN_POINT('',(4.00591003018116,-1.,-1.6));
#14448=CARTESIAN_POINT('',(4.00591003018116,-1.,-1.6));
#14449=CARTESIAN_POINT('Origin',(4.17091003018116,-1.,-1.6));
#14450=CARTESIAN_POINT('Origin',(4.17091003018116,-1.,-1.6));
#14451=CARTESIAN_POINT('',(3.77091003018116,-1.,-1.2));
#14452=CARTESIAN_POINT('Origin',(4.17091003018116,-1.,-1.2));
#14453=CARTESIAN_POINT('',(3.77091003018116,-1.,-1.6));
#14454=CARTESIAN_POINT('',(3.77091003018116,-1.,-1.6));
#14455=CARTESIAN_POINT('Origin',(4.17091003018116,-1.,-1.6));
#14456=CARTESIAN_POINT('Origin',(4.17091003018116,-1.,-1.2));
#14457=CARTESIAN_POINT('Origin',(4.17091003018116,-1.,-1.6));
#17741=UNCERTAINTY_MEASURE_WITH_UNIT(LENGTH_MEASURE(0.001),#17831,
'DISTANCE_ACCURACY_VALUE',
'Maximum model space distance between geometric entities at asserted c
onnectivities');
#17780=UNCERTAINTY_MEASURE_WITH_UNIT(LENGTH_MEASURE(0.001),#17831,
'DISTANCE_ACCURACY_VALUE',
'Maximum model space distance between geometric entities at asserted c
onnectivities');
#17791=(
GEOMETRIC_REPRESENTATION_CONTEXT(3)
GLOBAL_UNCERTAINTY_ASSIGNED_CONTEXT((#17741))
GLOBAL_UNIT_ASSIGNED_CONTEXT((#17831,#17833,#17834))
REPRESENTATION_CONTEXT('','3D')
);
#17830=(
GEOMETRIC_REPRESENTATION_CONTEXT(3)
GLOBAL_UNCERTAINTY_ASSIGNED_CONTEXT((#17780))
GLOBAL_UNIT_ASSIGNED_CONTEXT((#17831,#17833,#17834))
REPRESENTATION_CONTEXT('','3D')
);
#17831=(
LENGTH_UNIT()
NAMED_UNIT(*)
SI_UNIT(.CENTI.,.METRE.)
);
#17833=(
NAMED_UNIT(*)
PLANE_ANGLE_UNIT()
SI_UNIT($,.RADIAN.)
);
#17834=(
NAMED_UNIT(*)
SI_UNIT($,.STERADIAN.)
SOLID_ANGLE_UNIT()
);
#17845=SHAPE_DEFINITION_REPRESENTATION(#17894,#18016);
#17894=PRODUCT_DEFINITION_SHAPE('',$,#18066);
#18016=SHAPE_REPRESENTATION('',(#9744),#17791);
#18055=PRODUCT_DEFINITION_CONTEXT('part definition',#18204,'design');
#18066=PRODUCT_DEFINITION('M4 clamp nut','M4 clamp nut',#18115,#18055);
#18115=PRODUCT_DEFINITION_FORMATION('',$,#18216);
#18204=APPLICATION_CONTEXT(
'Core Data for Automotive Mechanical Design Process');
#18205=PRODUCT_CONTEXT('part definition',#18204,'mechanical');
#18216=PRODUCT('M4 clamp nut','M4 clamp nut','M4 clamp nut',(#18205));
#18318=COLOUR_RGB('Black',0.12,0.14,0.17);
#18319=FILL_AREA_STYLE_COLOUR('',#18318);
#18320=FILL_AREA_STYLE('',(#18319));
#18321=SURFACE_STYLE_FILL_AREA(#18320);
#18322=SURFACE_SIDE_STYLE('',(#18321));
#18323=SURFACE_STYLE_USAGE(.BOTH.,#18322);
#18324=PRESENTATION_STYLE_ASSIGNMENT((#18323));
ENDSEC;
END-ISO-10303-21;
